ISO-10303-21;
HEADER;
/* Generated by software containing ST-Developer
 * from STEP Tools, Inc. (www.steptools.com) 
 */

FILE_DESCRIPTION(
/* description */ (''),
/* implementation_level */ '2;1');

FILE_NAME(
/* name */ 'Cap_Screw_02.step',
/* time_stamp */ '2026-10-22T13:39:42+06:00',
/* author */ (''),
/* organization */ (''),
/* preprocessor_version */ 'ST-DEVELOPER v20.2',
/* originating_system */ 'Autodesk Translation Framework v15.15.0.0',
/* authorisation */ '');

FILE_SCHEMA (('AUTOMOTIVE_DESIGN { 1 0 10303 214 3 1 1 }'));
ENDSEC;

DATA;
#10=MECHANICAL_DESIGN_GEOMETRIC_PRESENTATION_REPRESENTATION('',(#314),#17836);
#294=SHAPE_REPRESENTATION_RELATIONSHIP('SRR','None',#17881,#304);
#304=ADVANCED_BREP_SHAPE_REPRESENTATION('',(#324),#17833);
#314=STYLED_ITEM('',(#17980),#324);
#324=MANIFOLD_SOLID_BREP('Cap_Screw_02',#9635);
#592=CYLINDRICAL_SURFACE('',#10819,9.);
#593=CYLINDRICAL_SURFACE('',#10823,7.5);
#1207=LINE('',#17395,#1872);
#1208=LINE('',#17399,#1873);
#1209=LINE('',#17403,#1874);
#1210=LINE('',#17406,#1875);
#1872=VECTOR('',#13737,8.5);
#1873=VECTOR('',#13742,9.);
#1874=VECTOR('',#13749,8.5);
#1875=VECTOR('',#13752,7.5);
#1972=CONICAL_SURFACE('',#10816,8.5,0.78539816339745);
#1973=CONICAL_SURFACE('',#10822,8.5,0.78539816339745);
#2022=FACE_BOUND('',#3203,.T.);
#2540=FACE_OUTER_BOUND('',#3202,.T.);
#2541=FACE_OUTER_BOUND('',#3204,.T.);
#2542=FACE_OUTER_BOUND('',#3205,.T.);
#2543=FACE_OUTER_BOUND('',#3206,.T.);
#2544=FACE_OUTER_BOUND('',#3207,.T.);
#2545=FACE_OUTER_BOUND('',#3208,.T.);
#2546=FACE_OUTER_BOUND('',#3209,.T.);
#3202=EDGE_LOOP('',(#8457));
#3203=EDGE_LOOP('',(#8458));
#3204=EDGE_LOOP('',(#8459,#8460,#8461,#8462));
#3205=EDGE_LOOP('',(#8463,#8464,#8465,#8466));
#3206=EDGE_LOOP('',(#8467));
#3207=EDGE_LOOP('',(#8468,#8469,#8470,#8471));
#3208=EDGE_LOOP('',(#8472,#8473,#8474,#8475));
#3209=EDGE_LOOP('',(#8476));
#3834=CIRCLE('',#10814,8.);
#3835=CIRCLE('',#10815,7.5);
#3836=CIRCLE('',#10817,8.);
#3837=CIRCLE('',#10818,9.);
#3838=CIRCLE('',#10820,9.);
#3839=CIRCLE('',#10824,7.5);
#4612=VERTEX_POINT('',#17387);
#4613=VERTEX_POINT('',#17389);
#4614=VERTEX_POINT('',#17392);
#4615=VERTEX_POINT('',#17394);
#4616=VERTEX_POINT('',#17398);
#4617=VERTEX_POINT('',#17405);
#5899=EDGE_CURVE('',#4612,#4612,#3834,.T.);
#5900=EDGE_CURVE('',#4613,#4613,#3835,.T.);
#5901=EDGE_CURVE('',#4614,#4614,#3836,.T.);
#5902=EDGE_CURVE('',#4614,#4615,#1207,.T.);
#5903=EDGE_CURVE('',#4615,#4615,#3837,.T.);
#5904=EDGE_CURVE('',#4615,#4616,#1208,.T.);
#5905=EDGE_CURVE('',#4616,#4616,#3838,.T.);
#5906=EDGE_CURVE('',#4616,#4612,#1209,.T.);
#5907=EDGE_CURVE('',#4613,#4617,#1210,.T.);
#5908=EDGE_CURVE('',#4617,#4617,#3839,.T.);
#8457=ORIENTED_EDGE('',*,*,#5899,.F.);
#8458=ORIENTED_EDGE('',*,*,#5900,.T.);
#8459=ORIENTED_EDGE('',*,*,#5901,.T.);
#8460=ORIENTED_EDGE('',*,*,#5902,.T.);
#8461=ORIENTED_EDGE('',*,*,#5903,.T.);
#8462=ORIENTED_EDGE('',*,*,#5902,.F.);
#8463=ORIENTED_EDGE('',*,*,#5903,.F.);
#8464=ORIENTED_EDGE('',*,*,#5904,.T.);
#8465=ORIENTED_EDGE('',*,*,#5905,.F.);
#8466=ORIENTED_EDGE('',*,*,#5904,.F.);
#8467=ORIENTED_EDGE('',*,*,#5901,.F.);
#8468=ORIENTED_EDGE('',*,*,#5905,.T.);
#8469=ORIENTED_EDGE('',*,*,#5906,.T.);
#8470=ORIENTED_EDGE('',*,*,#5899,.T.);
#8471=ORIENTED_EDGE('',*,*,#5906,.F.);
#8472=ORIENTED_EDGE('',*,*,#5900,.F.);
#8473=ORIENTED_EDGE('',*,*,#5907,.T.);
#8474=ORIENTED_EDGE('',*,*,#5908,.T.);
#8475=ORIENTED_EDGE('',*,*,#5907,.F.);
#8476=ORIENTED_EDGE('',*,*,#5908,.F.);
#8991=PLANE('',#10813);
#8992=PLANE('',#10821);
#8993=PLANE('',#10825);
#9527=ADVANCED_FACE('',(#2540,#2022),#8991,.F.);
#9528=ADVANCED_FACE('',(#2541),#1972,.T.);
#9529=ADVANCED_FACE('',(#2542),#592,.T.);
#9530=ADVANCED_FACE('',(#2543),#8992,.T.);
#9531=ADVANCED_FACE('',(#2544),#1973,.T.);
#9532=ADVANCED_FACE('',(#2545),#593,.T.);
#9533=ADVANCED_FACE('',(#2546),#8993,.F.);
#9635=CLOSED_SHELL('',(#9527,#9528,#9529,#9530,#9531,#9532,#9533));
#10812=AXIS2_PLACEMENT_3D('',#17385,#13725,#13726);
#10813=AXIS2_PLACEMENT_3D('',#17386,#13727,#13728);
#10814=AXIS2_PLACEMENT_3D('',#17388,#13729,#13730);
#10815=AXIS2_PLACEMENT_3D('',#17390,#13731,#13732);
#10816=AXIS2_PLACEMENT_3D('',#17391,#13733,#13734);
#10817=AXIS2_PLACEMENT_3D('',#17393,#13735,#13736);
#10818=AXIS2_PLACEMENT_3D('',#17396,#13738,#13739);
#10819=AXIS2_PLACEMENT_3D('',#17397,#13740,#13741);
#10820=AXIS2_PLACEMENT_3D('',#17400,#13743,#13744);
#10821=AXIS2_PLACEMENT_3D('',#17401,#13745,#13746);
#10822=AXIS2_PLACEMENT_3D('',#17402,#13747,#13748);
#10823=AXIS2_PLACEMENT_3D('',#17404,#13750,#13751);
#10824=AXIS2_PLACEMENT_3D('',#17407,#13753,#13754);
#10825=AXIS2_PLACEMENT_3D('',#17408,#13755,#13756);
#13725=DIRECTION('axis',(0.,0.,1.));
#13726=DIRECTION('refdir',(1.,0.,0.));
#13727=DIRECTION('center_axis',(-1.,2.22044604925031E-16,0.));
#13728=DIRECTION('ref_axis',(-2.22044604925031E-16,-1.,0.));
#13729=DIRECTION('center_axis',(-1.,2.22044604925031E-16,0.));
#13730=DIRECTION('ref_axis',(-2.22044604925031E-16,-1.,0.));
#13731=DIRECTION('center_axis',(-1.,2.22044604925031E-16,0.));
#13732=DIRECTION('ref_axis',(-2.22044604925031E-16,-1.,0.));
#13733=DIRECTION('center_axis',(1.,-2.22044604925031E-16,0.));
#13734=DIRECTION('ref_axis',(-2.22044604925031E-16,-1.,0.));
#13735=DIRECTION('center_axis',(1.,-2.22044604925031E-16,0.));
#13736=DIRECTION('ref_axis',(-2.22044604925031E-16,-1.,0.));
#13737=DIRECTION('',(0.707106781186547,0.707106781186549,-8.65956056235495E-17));
#13738=DIRECTION('center_axis',(-1.,2.22044604925031E-16,0.));
#13739=DIRECTION('ref_axis',(-2.22044604925031E-16,-1.,0.));
#13740=DIRECTION('center_axis',(-1.,2.22044604925031E-16,0.));
#13741=DIRECTION('ref_axis',(-2.22044604925031E-16,-1.,0.));
#13742=DIRECTION('',(1.,-2.22044604925031E-16,0.));
#13743=DIRECTION('center_axis',(1.,-2.22044604925031E-16,0.));
#13744=DIRECTION('ref_axis',(-2.22044604925031E-16,-1.,0.));
#13745=DIRECTION('center_axis',(-1.,2.22044604925031E-16,0.));
#13746=DIRECTION('ref_axis',(-2.22044604925031E-16,-1.,0.));
#13747=DIRECTION('center_axis',(-1.,2.22044604925031E-16,0.));
#13748=DIRECTION('ref_axis',(-2.22044604925031E-16,-1.,0.));
#13749=DIRECTION('',(0.707106781186546,-0.707106781186549,8.65956056235495E-17));
#13750=DIRECTION('center_axis',(-1.,2.22044604925031E-16,0.));
#13751=DIRECTION('ref_axis',(-2.22044604925031E-16,-1.,0.));
#13752=DIRECTION('',(1.,-2.22044604925031E-16,0.));
#13753=DIRECTION('center_axis',(-1.,2.22044604925031E-16,0.));
#13754=DIRECTION('ref_axis',(-2.22044604925031E-16,-1.,0.));
#13755=DIRECTION('center_axis',(-1.,2.22044604925031E-16,0.));
#13756=DIRECTION('ref_axis',(-2.22044604925031E-16,-1.,0.));
#17385=CARTESIAN_POINT('',(0.,0.,0.));
#17386=CARTESIAN_POINT('Origin',(-115.,1.77635683940025E-14,49.8489128715187));
#17387=CARTESIAN_POINT('',(-115.,8.00000000000002,49.8489128715187));
#17388=CARTESIAN_POINT('Origin',(-115.,1.77635683940025E-14,49.8489128715187));
#17389=CARTESIAN_POINT('',(-115.,7.50000000000002,49.8489128715187));
#17390=CARTESIAN_POINT('Origin',(-115.,1.77635683940025E-14,49.8489128715187));
#17391=CARTESIAN_POINT('Origin',(-134.5,5.32907051820075E-14,49.8489128715187));
#17392=CARTESIAN_POINT('',(-135.,8.00000000000004,49.8489128715187));
#17393=CARTESIAN_POINT('Origin',(-135.,5.32907051820075E-14,49.8489128715187));
#17394=CARTESIAN_POINT('',(-134.,9.00000000000004,49.8489128715187));
#17395=CARTESIAN_POINT('',(-134.5,8.50000000000005,49.8489128715187));
#17396=CARTESIAN_POINT('Origin',(-134.,5.32907051820075E-14,49.8489128715187));
#17397=CARTESIAN_POINT('Origin',(-115.,1.77635683940025E-14,49.8489128715187));
#17398=CARTESIAN_POINT('',(-116.,9.00000000000002,49.8489128715187));
#17399=CARTESIAN_POINT('',(-115.,9.00000000000002,49.8489128715187));
#17400=CARTESIAN_POINT('Origin',(-116.,1.77635683940025E-14,49.8489128715187));
#17401=CARTESIAN_POINT('Origin',(-135.,5.32907051820075E-14,49.8489128715187));
#17402=CARTESIAN_POINT('Origin',(-115.5,1.77635683940025E-14,49.8489128715187));
#17403=CARTESIAN_POINT('',(-115.5,8.50000000000002,49.8489128715187));
#17404=CARTESIAN_POINT('Origin',(-90.,1.77635683940025E-14,49.8489128715187));
#17405=CARTESIAN_POINT('',(-90.,7.50000000000002,49.8489128715187));
#17406=CARTESIAN_POINT('',(-90.,7.50000000000002,49.8489128715187));
#17407=CARTESIAN_POINT('Origin',(-90.,1.77635683940025E-14,49.8489128715187));
#17408=CARTESIAN_POINT('Origin',(-90.,1.77635683940025E-14,49.8489128715187));
#17821=UNCERTAINTY_MEASURE_WITH_UNIT(LENGTH_MEASURE(0.01),#17837,
'DISTANCE_ACCURACY_VALUE',
'Maximum model space distance between geometric entities at asserted c
onnectivities');
#17824=UNCERTAINTY_MEASURE_WITH_UNIT(LENGTH_MEASURE(0.01),#17837,
'DISTANCE_ACCURACY_VALUE',
'Maximum model space distance between geometric entities at asserted c
onnectivities');
#17833=(
GEOMETRIC_REPRESENTATION_CONTEXT(3)
GLOBAL_UNCERTAINTY_ASSIGNED_CONTEXT((#17821))
GLOBAL_UNIT_ASSIGNED_CONTEXT((#17837,#17839,#17840))
REPRESENTATION_CONTEXT('','3D')
);
#17836=(
GEOMETRIC_REPRESENTATION_CONTEXT(3)
GLOBAL_UNCERTAINTY_ASSIGNED_CONTEXT((#17824))
GLOBAL_UNIT_ASSIGNED_CONTEXT((#17837,#17839,#17840))
REPRESENTATION_CONTEXT('','3D')
);
#17837=(
LENGTH_UNIT()
NAMED_UNIT(*)
SI_UNIT(.MILLI.,.METRE.)
);
#17839=(
NAMED_UNIT(*)
PLANE_ANGLE_UNIT()
SI_UNIT($,.RADIAN.)
);
#17840=(
NAMED_UNIT(*)
SI_UNIT($,.STERADIAN.)
SOLID_ANGLE_UNIT()
);
#17849=SHAPE_DEFINITION_REPRESENTATION(#17860,#17881);
#17860=PRODUCT_DEFINITION_SHAPE('',$,#17893);
#17881=SHAPE_REPRESENTATION('',(#10812),#17833);
#17884=PRODUCT_DEFINITION_CONTEXT('part definition',#17919,'design');
#17893=PRODUCT_DEFINITION('Cap_Screw_02','Cap_Screw_02',#17904,#17884);
#17904=PRODUCT_DEFINITION_FORMATION('',$,#17929);
#17919=APPLICATION_CONTEXT(
'Core Data for Automotive Mechanical Design Process');
#17920=PRODUCT_CONTEXT('part definition',#17919,'mechanical');
#17929=PRODUCT('Cap_Screw_02','Cap_Screw_02',$,(#17920));
#17974=COLOUR_RGB('Black',0.12,0.14,0.17);
#17975=FILL_AREA_STYLE_COLOUR('',#17974);
#17976=FILL_AREA_STYLE('',(#17975));
#17977=SURFACE_STYLE_FILL_AREA(#17976);
#17978=SURFACE_SIDE_STYLE('',(#17977));
#17979=SURFACE_STYLE_USAGE(.BOTH.,#17978);
#17980=PRESENTATION_STYLE_ASSIGNMENT((#17979));
ENDSEC;
END-ISO-10303-21;
